ISO-10303-21;
HEADER;
FILE_DESCRIPTION (('STEP AP214'),
    '1' );
FILE_NAME ('socket head cap screw_iso_ISO 4762 M4 x 10 - 10N.step',
    '2026-10-31T03:44:21',
    ( '' ),
    ( '' ),
    'SwSTEP 2.0',
    'SolidWorks 2026',
    '' );
FILE_SCHEMA (( 'AUTOMOTIVE_DESIGN' ));
ENDSEC;

DATA;
#24=VECTOR ( 'NONE', #9487, 1000.000000000000000 ) ;
#41=AXIS2_PLACEMENT_3D ( 'NONE', #5038, #18489, #12385 ) ;
#42=CARTESIAN_POINT ( 'NONE',  ( 13.99999999999999822, 0.000000000000000000, 0.000000000000000000 ) ) ;
#100=UNCERTAINTY_MEASURE_WITH_UNIT (LENGTH_MEASURE( 1.000000000000000082E-05 ), #14123, 'distance_accuracy_value', 'NONE');
#130=AXIS2_PLACEMENT_3D ( 'NONE', #17222, #3785, #15743 ) ;
#138=ORIENTED_EDGE ( 'NONE', *, *, #15996, .F. ) ;
#182=SURFACE_STYLE_USAGE ( .BOTH. , #380 ) ;
#194=DIRECTION ( 'NONE',  ( -1.000000000000000000, -0.000000000000000000, -0.000000000000000000 ) ) ;
#197=CARTESIAN_POINT ( 'NONE',  ( 0.000000000000000000, 4.163799117101000559E-16, -3.299999999999999822 ) ) ;
#201=CARTESIAN_POINT ( 'NONE',  ( 2.000000000000000000, 1.773042676681340524, -2.059984127722458425E-15 ) ) ;
#206=VERTEX_POINT ( 'NONE', #16694 ) ;
#217=DIRECTION ( 'NONE',  ( 0.000000000000000000, 0.000000000000000000, 1.000000000000000000 ) ) ;
#271=ORIENTED_EDGE ( 'NONE', *, *, #6050, .F. ) ;
#298=CARTESIAN_POINT ( 'NONE',  ( 2.000000000000000000, 0.000000000000000000, 1.535500000000000087 ) ) ;
#314=DIRECTION ( 'NONE',  ( -1.000000000000000000, -0.000000000000000000, -0.000000000000000000 ) ) ;
#367=AXIS2_PLACEMENT_3D ( 'NONE', #6405, #16916, #9445 ) ;
#380=SURFACE_SIDE_STYLE ('',( #4792 ) ) ;
#440=VERTEX_POINT ( 'NONE', #7521 ) ;
#463=SHAPE_REPRESENTATION_RELATIONSHIP ( 'NONE' , 'NONE' ,  #10550, #17389 ) ;
#473=EDGE_LOOP ( 'NONE', ( #18813, #10177, #17658, #2063, #11824 ) ) ;
#475=UNCERTAINTY_MEASURE_WITH_UNIT (LENGTH_MEASURE( 1.000000000000000082E-05 ), #13517, 'distance_accuracy_value', 'NONE');
#530=ORIENTED_EDGE ( 'NONE', *, *, #763, .F. ) ;
#581=ORIENTED_EDGE ( 'NONE', *, *, #17054, .F. ) ;
#584=CARTESIAN_POINT ( 'NONE',  ( -31.74999999999995737, 0.000000000000000000, 0.000000000000000000 ) ) ;
#604=CARTESIAN_POINT ( 'NONE',  ( 2.000000000000000000, 1.773042676681340524, -2.059984127722458425E-15 ) ) ;
#679=LINE ( 'NONE', #298, #24 ) ;
#739=FACE_OUTER_BOUND ( 'NONE', #15662, .T. ) ;
#760=EDGE_LOOP ( 'NONE', ( #5028, #7175, #2540, #12004 ) ) ;
#763=EDGE_CURVE ( 'NONE', #10243, #10468, #4266, .T. ) ;
#769=DIRECTION ( 'NONE',  ( -0.000000000000000000, 0.8660254037844392627, 0.4999999999999990008 ) ) ;
#789=ADVANCED_FACE ( 'NONE', ( #5437, #16232 ), #11611, .T. ) ;
#819=EDGE_CURVE ( 'NONE', #6895, #18142, #941, .T. ) ;
#850=FACE_OUTER_BOUND ( 'NONE', #6828, .T. ) ;
#897=CIRCLE ( 'NONE', #2165, 1.535500000000000087 ) ;
#920=CARTESIAN_POINT ( 'NONE',  ( 13.61000000000001009, 0.000000000000000000, 2.000000000000001332 ) ) ;
#921=EDGE_LOOP ( 'NONE', ( #10443, #9590, #15952, #12832 ) ) ;
#936=EDGE_LOOP ( 'NONE', ( #5155, #11862, #5868, #11722 ) ) ;
#941=LINE ( 'NONE', #10137, #9151 ) ;
#1001=EDGE_CURVE ( 'NONE', #7143, #16099, #3099, .T. ) ;
#1013=DIRECTION ( 'NONE',  ( 0.000000000000000000, 0.8660254037844380415, -0.5000000000000012212 ) ) ;
#1117=CARTESIAN_POINT ( 'NONE',  ( -31.74999999999995737, 0.000000000000000000, 0.000000000000000000 ) ) ;
#1137=CIRCLE ( 'NONE', #8640, 3.500000000000000000 ) ;
#1240=DIRECTION ( 'NONE',  ( 0.000000000000000000, 0.000000000000000000, 1.000000000000000000 ) ) ;
#1357=DIRECTION ( 'NONE',  ( 0.000000000000000000, 0.000000000000000000, -1.000000000000000000 ) ) ;
#1388=EDGE_CURVE ( 'NONE', #18424, #2267, #13694, .T. ) ;
#1392=EDGE_CURVE ( 'NONE', #15249, #6396, #13991, .T. ) ;
#1400=FACE_OUTER_BOUND ( 'NONE', #15730, .T. ) ;
#1426=CARTESIAN_POINT ( 'NONE',  ( 2.000000000000000000, 0.8865213383406715941, 1.535499999999999199 ) ) ;
#1427=CARTESIAN_POINT ( 'NONE',  ( 2.000000000000000000, -1.329782007511007169, -0.7677499999999988223 ) ) ;
#1479=CARTESIAN_POINT ( 'NONE',  ( 2.000000000000000000, -1.773042676681341856, 2.276824562219559311E-15 ) ) ;
#1494=ADVANCED_FACE ( 'NONE', ( #1400 ), #5241, .F. ) ;
#1502=AXIS2_PLACEMENT_3D ( 'NONE', #10696, #16600, #13253 ) ;
#1503=DIRECTION ( 'NONE',  ( 0.000000000000000000, 0.000000000000000000, 1.000000000000000000 ) ) ;
#1519=FACE_OUTER_BOUND ( 'NONE', #5287, .T. ) ;
#1559=ORIENTED_EDGE ( 'NONE', *, *, #7937, .F. ) ;
#1566=CARTESIAN_POINT ( 'NONE',  ( 4.000000000000003553, 0.000000000000000000, 3.500000000000000000 ) ) ;
#1568=AXIS2_PLACEMENT_3D ( 'NONE', #1117, #12971, #18979 ) ;
#1587=PRODUCT_CONTEXT ( 'NONE', #4879, 'mechanical' ) ;
#1685=DIRECTION ( 'NONE',  ( -1.000000000000000000, -0.000000000000000000, -0.000000000000000000 ) ) ;
#1687=EDGE_LOOP ( 'NONE', ( #4671, #16930, #7091 ) ) ;
#1746=ADVANCED_FACE ( 'NONE', ( #11559 ), #5589, .F. ) ;
#1757=ADVANCED_FACE ( 'NONE', ( #3837 ), #8625, .T. ) ;
#1775=FACE_OUTER_BOUND ( 'NONE', #921, .T. ) ;
#1842=AXIS2_PLACEMENT_3D ( 'NONE', #12809, #8386, #5449 ) ;
#1846=EDGE_CURVE ( 'NONE', #18783, #9833, #1137, .T. ) ;
#1859=CONICAL_SURFACE ( 'NONE', #1842, 1.535500000000000087, 1.047197551196590748 ) ;
#1917=CONICAL_SURFACE ( 'NONE', #13170, 1.610000000000000098, 0.7853981633974658205 ) ;
#2001=DIRECTION ( 'NONE',  ( -1.000000000000000000, -0.000000000000000000, -0.000000000000000000 ) ) ;
#2008=AXIS2_PLACEMENT_3D ( 'NONE', #3974, #14545, #4169 ) ;
#2038=EDGE_LOOP ( 'NONE', ( #8946, #15241, #19336, #1559 ) ) ;
#2043=EDGE_LOOP ( 'NONE', ( #9607, #6346 ) ) ;
#2063=ORIENTED_EDGE ( 'NONE', *, *, #7478, .F. ) ;
#2145=CARTESIAN_POINT ( 'NONE',  ( 4.000000000000001776, 2.694222958124178486E-16, 2.200000000000001066 ) ) ;
#2165=AXIS2_PLACEMENT_3D ( 'NONE', #6435, #13696, #16664 ) ;
#2215=ADVANCED_FACE ( 'NONE', ( #7035 ), #14385, .T. ) ;
#2241=ADVANCED_FACE ( 'NONE', ( #12828 ), #12923, .T. ) ;
#2244=FACE_OUTER_BOUND ( 'NONE', #4186, .T. ) ;
#2258=DIRECTION ( 'NONE',  ( -1.000000000000000000, -0.000000000000000000, -0.000000000000000000 ) ) ;
#2267=VERTEX_POINT ( 'NONE', #16264 ) ;
#2291=( NAMED_UNIT ( * ) PLANE_ANGLE_UNIT ( ) SI_UNIT ( $, .RADIAN. ) );
#2295=CARTESIAN_POINT ( 'NONE',  ( 2.000000000000000000, 1.773042676681340524, -2.059984127722458425E-15 ) ) ;
#2314=ORIENTED_EDGE ( 'NONE', *, *, #7282, .F. ) ;
#2317=ORIENTED_EDGE ( 'NONE', *, *, #16458, .T. ) ;
#2380=DIRECTION ( 'NONE',  ( -0.000000000000000000, 1.000000000000000000, 1.224646799147353207E-16 ) ) ;
#2396=DIRECTION ( 'NONE',  ( 0.000000000000000000, 0.4999999999999989453, -0.8660254037844391517 ) ) ;
#2430=LINE ( 'NONE', #8381, #6912 ) ;
#2493=FACE_OUTER_BOUND ( 'NONE', #2738, .T. ) ;
#2504=CARTESIAN_POINT ( 'NONE',  ( 0.1999999999999987899, 0.000000000000000000, 0.000000000000000000 ) ) ;
#2540=ORIENTED_EDGE ( 'NONE', *, *, #11678, .T. ) ;
#2570=ADVANCED_FACE ( 'NONE', ( #2695 ), #16027, .T. ) ;
#2575=VECTOR ( 'NONE', #10158, 1000.000000000000000 ) ;
#2592=EDGE_CURVE ( 'NONE', #3495, #7143, #10019, .T. ) ;
#2594=ADVANCED_FACE ( 'NONE', ( #4243 ), #8649, .T. ) ;
#2643=CARTESIAN_POINT ( 'NONE',  ( 2.000000000000000000, 1.329782007511004727, -0.7677500000000018199 ) ) ;
#2655=ADVANCED_FACE ( 'NONE', ( #10410 ), #4340, .F. ) ;
#2695=FACE_OUTER_BOUND ( 'NONE', #8011, .T. ) ;
#2726=ORIENTED_EDGE ( 'NONE', *, *, #5478, .F. ) ;
#2727=ORIENTED_EDGE ( 'NONE', *, *, #6989, .T. ) ;
#2738=EDGE_LOOP ( 'NONE', ( #12306, #18684, #5042, #5138, #9261 ) ) ;
#2742=VECTOR ( 'NONE', #12153, 1000.000000000000000 ) ;
#2797=FACE_OUTER_BOUND ( 'NONE', #5969, .T. ) ;
#2871=CARTESIAN_POINT ( 'NONE',  ( 0.000000000000000000, 0.000000000000000000, 0.000000000000000000 ) ) ;
#2896=CARTESIAN_POINT ( 'NONE',  ( 0.000000000000000000, 0.8865213383406715941, 1.535499999999999199 ) ) ;
#2902=DIRECTION ( 'NONE',  ( 0.000000000000000000, 1.000000000000000000, -1.345283343056720273E-15 ) ) ;
#2919=ORIENTED_EDGE ( 'NONE', *, *, #14071, .T. ) ;
#2954=PLANE ( 'NONE',  #12880 ) ;
#2978=EDGE_CURVE ( 'NONE', #6396, #15249, #9141, .T. ) ;
#2995=LINE ( 'NONE', #16522, #5436 ) ;
#3099=LINE ( 'NONE', #1426, #19207 ) ;
#3111=CIRCLE ( 'NONE', #18453, 1.535500000000000087 ) ;
#3135=VERTEX_POINT ( 'NONE', #7899 ) ;
#3172=DIRECTION ( 'NONE',  ( -1.000000000000000000, -0.000000000000000000, -0.000000000000000000 ) ) ;
#3174=ADVANCED_FACE ( 'NONE', ( #739 ), #5243, .F. ) ;
#3215=CARTESIAN_POINT ( 'NONE',  ( 0.000000000000000000, -0.8865213383406694847, 1.535500000000001419 ) ) ;
#3222=EDGE_CURVE ( 'NONE', #206, #18916, #17044, .T. ) ;
#3239=UNCERTAINTY_MEASURE_WITH_UNIT (LENGTH_MEASURE( 1.000000000000000082E-05 ), #11941, 'distance_accuracy_value', 'NONE');
#3335=ADVANCED_FACE ( 'NONE', ( #10518, #1519 ), #6032, .T. ) ;
#3368=DIRECTION ( 'NONE',  ( -0.7071067811865350272, 8.659560562355083235E-17, -0.7071067811865598962 ) ) ;
#3413=EDGE_CURVE ( 'NONE', #14560, #8619, #2995, .T. ) ;
#3480=FACE_OUTER_BOUND ( 'NONE', #473, .T. ) ;
#3495=VERTEX_POINT ( 'NONE', #13568 ) ;
#3512=CARTESIAN_POINT ( 'NONE',  ( 4.200000000000001954, 2.449293598294707893E-16, -2.000000000000000888 ) ) ;
#3524=DIRECTION ( 'NONE',  ( 0.000000000000000000, 0.000000000000000000, 1.000000000000000000 ) ) ;
#3544=EDGE_CURVE ( 'NONE', #6895, #16099, #13754, .T. ) ;
#3546=EDGE_CURVE ( 'NONE', #10132, #10468, #3583, .T. ) ;
#3583=CIRCLE ( 'NONE', #15471, 1.535500000000000087 ) ;
#3623=LINE ( 'NONE', #6557, #15017 ) ;
#3671=AXIS2_PLACEMENT_3D ( 'NONE', #18629, #2258, #12918 ) ;
#3733=CARTESIAN_POINT ( 'NONE',  ( 4.000000000000003553, 0.000000000000000000, 0.000000000000000000 ) ) ;
#3751=PLANE ( 'NONE',  #16530 ) ;
#3759=EDGE_CURVE ( 'NONE', #8619, #9062, #16203, .T. ) ;
#3785=DIRECTION ( 'NONE',  ( 1.000000000000000000, 0.000000000000000000, 0.000000000000000000 ) ) ;
#3794=EDGE_CURVE ( 'NONE', #14540, #4021, #8453, .T. ) ;
#3806=CIRCLE ( 'NONE', #41, 1.535500000000000087 ) ;
#3821=AXIS2_PLACEMENT_3D ( 'NONE', #19273, #5812, #7082 ) ;
#3837=FACE_OUTER_BOUND ( 'NONE', #760, .T. ) ;
#3847=LINE ( 'NONE', #12760, #5472 ) ;
#3853=DIRECTION ( 'NONE',  ( -1.000000000000000000, -0.000000000000000000, -0.000000000000000000 ) ) ;
#3920=( GEOMETRIC_REPRESENTATION_CONTEXT ( 3 ) GLOBAL_UNCERTAINTY_ASSIGNED_CONTEXT ( ( #100 ) ) GLOBAL_UNIT_ASSIGNED_CONTEXT ( ( #14123, #2291, #17288 ) ) REPRESENTATION_CONTEXT ( 'NONE', 'WORKASPACE' ) );
#3942=ORIENTED_EDGE ( 'NONE', *, *, #13805, .F. ) ;
#3974=CARTESIAN_POINT ( 'NONE',  ( 13.61000000000001009, 0.000000000000000000, 0.000000000000000000 ) ) ;
#4016=ORIENTED_EDGE ( 'NONE', *, *, #9681, .F. ) ;
#4017=CARTESIAN_POINT ( 'NONE',  ( 2.000000000000000000, 1.773042676681340524, -2.059984127722458425E-15 ) ) ;
#4021=VERTEX_POINT ( 'NONE', #6669 ) ;
#4043=( GEOMETRIC_REPRESENTATION_CONTEXT ( 3 ) GLOBAL_UNCERTAINTY_ASSIGNED_CONTEXT ( ( #3239 ) ) GLOBAL_UNIT_ASSIGNED_CONTEXT ( ( #11941, #8995, #9095 ) ) REPRESENTATION_CONTEXT ( 'NONE', 'WORKASPACE' ) );
#4065=AXIS2_PLACEMENT_3D ( 'NONE', #584, #18259, #12542 ) ;
#4157=DIRECTION ( 'NONE',  ( -1.000000000000000000, -0.000000000000000000, -0.000000000000000000 ) ) ;
#4169=DIRECTION ( 'NONE',  ( 0.000000000000000000, 0.000000000000000000, 1.000000000000000000 ) ) ;
#4178=ORIENTED_EDGE ( 'NONE', *, *, #7820, .T. ) ;
#4186=EDGE_LOOP ( 'NONE', ( #530, #16037, #5136, #18918, #10560 ) ) ;
#4207=DIRECTION ( 'NONE',  ( 0.000000000000000000, 1.000000000000000000, -1.224646799147353207E-16 ) ) ;
#4243=FACE_OUTER_BOUND ( 'NONE', #18627, .T. ) ;
#4266=LINE ( 'NONE', #7202, #6966 ) ;
#4297=PRODUCT ( 'socket head cap screw_iso_ISO 4762 M4 x 10 - 10N', 'socket head cap screw_iso_ISO 4762 M4 x 10 - 10N', '', ( #1587 ) ) ;
#4336=DIRECTION ( 'NONE',  ( 0.000000000000000000, 0.000000000000000000, -1.000000000000000000 ) ) ;
#4338=CARTESIAN_POINT ( 'NONE',  ( 0.000000000000000000, 0.000000000000000000, 0.000000000000000000 ) ) ;
#4340=PLANE ( 'NONE',  #4442 ) ;
#4385=ORIENTED_EDGE ( 'NONE', *, *, #12987, .T. ) ;
#4442=AXIS2_PLACEMENT_3D ( 'NONE', #12076, #9035, #6018 ) ;
#4464=CARTESIAN_POINT ( 'NONE',  ( 4.000000000000000000, 3.500000000000000000, 0.000000000000000000 ) ) ;
#4472=ORIENTED_EDGE ( 'NONE', *, *, #12996, .F. ) ;
#4476=ORIENTED_EDGE ( 'NONE', *, *, #7820, .F. ) ;
#4570=AXIS2_PLACEMENT_3D ( 'NONE', #17353, #5276, #15676 ) ;
#4620=DIRECTION ( 'NONE',  ( 0.000000000000000000, 0.000000000000000000, 1.000000000000000000 ) ) ;
#4627=VERTEX_POINT ( 'NONE', #197 ) ;
#4657=DIRECTION ( 'NONE',  ( 1.000000000000000000, 0.000000000000000000, 0.000000000000000000 ) ) ;
#4671=ORIENTED_EDGE ( 'NONE', *, *, #19370, .F. ) ;
#4675=DIRECTION ( 'NONE',  ( 0.000000000000000000, -1.000000000000000000, 0.000000000000000000 ) ) ;
#4686=DIRECTION ( 'NONE',  ( 0.000000000000000000, 0.000000000000000000, -1.000000000000000000 ) ) ;
#4713=DIRECTION ( 'NONE',  ( 0.000000000000000000, -0.4999999999999991118, 0.8660254037844391517 ) ) ;
#4720=CARTESIAN_POINT ( 'NONE',  ( 2.000000000000000000, -0.8865213383406694847, 1.535500000000001419 ) ) ;
#4746=AXIS2_PLACEMENT_3D ( 'NONE', #11340, #14766, #9959 ) ;
#4758=DIRECTION ( 'NONE',  ( -1.000000000000000000, -0.000000000000000000, -0.000000000000000000 ) ) ;
#4792=SURFACE_STYLE_FILL_AREA ( #16665 ) ;
#4814=FACE_OUTER_BOUND ( 'NONE', #10938, .T. ) ;
#4853=STYLED_ITEM('',(#19475),#8977);
#4878=DIRECTION ( 'NONE',  ( 0.000000000000000000, 1.000000000000000000, -9.783878858594328898E-16 ) ) ;
#4879=APPLICATION_CONTEXT ( 'automotive_design' ) ;
#4905=ORIENTED_EDGE ( 'NONE', *, *, #13922, .T. ) ;
#4916=CIRCLE ( 'NONE', #5230, 1.535500000000000087 ) ;
#4934=AXIS2_PLACEMENT_3D ( 'NONE', #13039, #15892, #17277 ) ;
#5028=ORIENTED_EDGE ( 'NONE', *, *, #6748, .F. ) ;
#5030=CARTESIAN_POINT ( 'NONE',  ( 0.000000000000000000, 1.773042676681340524, -2.059984127722458425E-15 ) ) ;
#5038=CARTESIAN_POINT ( 'NONE',  ( 2.000000000000000000, 0.000000000000000000, 0.000000000000000000 ) ) ;
#5042=ORIENTED_EDGE ( 'NONE', *, *, #19370, .T. ) ;
#5053=ORIENTED_EDGE ( 'NONE', *, *, #6989, .F. ) ;
#5084=AXIS2_PLACEMENT_3D ( 'NONE', #14547, #7007, #12898 ) ;
#5132=VECTOR ( 'NONE', #16698, 1000.000000000000000 ) ;
#5136=ORIENTED_EDGE ( 'NONE', *, *, #13805, .T. ) ;
#5138=ORIENTED_EDGE ( 'NONE', *, *, #5939, .T. ) ;
#5155=ORIENTED_EDGE ( 'NONE', *, *, #9324, .T. ) ;
#5162=VERTEX_POINT ( 'NONE', #8255 ) ;
#5230=AXIS2_PLACEMENT_3D ( 'NONE', #16764, #194, #6358 ) ;
#5241=TOROIDAL_SURFACE ( 'NONE', #1502, 2.200000000000001066, 0.2000000000000000111 ) ;
#5243=PLANE ( 'NONE',  #130 ) ;
#5264=EDGE_LOOP ( 'NONE', ( #12609, #6249, #3942 ) ) ;
#5276=DIRECTION ( 'NONE',  ( 1.000000000000000000, 0.000000000000000000, 0.000000000000000000 ) ) ;
#5278=( GEOMETRIC_REPRESENTATION_CONTEXT ( 3 ) GLOBAL_UNCERTAINTY_ASSIGNED_CONTEXT ( ( #475 ) ) GLOBAL_UNIT_ASSIGNED_CONTEXT ( ( #13517, #18328, #10556 ) ) REPRESENTATION_CONTEXT ( 'NONE', 'WORKASPACE' ) );
#5287=EDGE_LOOP ( 'NONE', ( #271, #13766 ) ) ;
#5314=ORIENTED_EDGE ( 'NONE', *, *, #16458, .F. ) ;
#5363=VECTOR ( 'NONE', #16546, 1000.000000000000000 ) ;
#5375=EDGE_CURVE ( 'NONE', #10468, #9062, #16503, .T. ) ;
#5381=ORIENTED_EDGE ( 'NONE', *, *, #12215, .T. ) ;
#5436=VECTOR ( 'NONE', #7396, 1000.000000000000227 ) ;
#5437=FACE_BOUND ( 'NONE', #14077, .T. ) ;
#5449=DIRECTION ( 'NONE',  ( 0.000000000000000000, 0.000000000000000000, 1.000000000000000000 ) ) ;
#5472=VECTOR ( 'NONE', #9520, 1000.000000000000227 ) ;
#5478=EDGE_CURVE ( 'NONE', #3135, #4627, #17603, .T. ) ;
#5494=PLANE ( 'NONE',  #12512 ) ;
#5589=PLANE ( 'NONE',  #4934 ) ;
#5595=DIRECTION ( 'NONE',  ( 1.000000000000000000, 0.000000000000000000, 0.000000000000000000 ) ) ;
#5609=AXIS2_PLACEMENT_3D ( 'NONE', #42, #16126, #17896 ) ;
#5622=CYLINDRICAL_SURFACE ( 'NONE', #1568, 3.500000000000000000 ) ;
#5635=DIRECTION ( 'NONE',  ( -0.5000000000000061062, 1.060575238724902601E-16, -0.8660254037844351549 ) ) ;
#5707=PRODUCT_DEFINITION_SHAPE ( 'NONE', 'NONE',  #14639 ) ;
#5728=VERTEX_POINT ( 'NONE', #12942 ) ;
#5756=EDGE_LOOP ( 'NONE', ( #14976, #4476, #17749, #4016, #12995 ) ) ;
#5793=CARTESIAN_POINT ( 'NONE',  ( 2.000000000000000000, -0.8865213383406694847, 1.535500000000001419 ) ) ;
#5812=DIRECTION ( 'NONE',  ( 0.000000000000000000, 0.8660254037844380415, -0.5000000000000012212 ) ) ;
#5868=ORIENTED_EDGE ( 'NONE', *, *, #1392, .T. ) ;
#5871=ADVANCED_FACE ( 'NONE', ( #9012 ), #16389, .T. ) ;
#5914=ADVANCED_FACE ( 'NONE', ( #10388 ), #2954, .F. ) ;
#5917=CARTESIAN_POINT ( 'NONE',  ( 2.000000000000000000, -1.773042676681341856, 2.276824562219559311E-15 ) ) ;
#5939=EDGE_CURVE ( 'NONE', #6090, #7143, #16579, .T. ) ;
#5969=EDGE_LOOP ( 'NONE', ( #10642, #11814, #14582, #17945 ) ) ;
#6018=DIRECTION ( 'NONE',  ( 0.000000000000000000, 0.000000000000000000, -1.000000000000000000 ) ) ;
#6020=CARTESIAN_POINT ( 'NONE',  ( -31.74999999999995737, 4.286263797015736595E-16, -3.500000000000000000 ) ) ;
#6032=PLANE ( 'NONE',  #16102 ) ;
#6050=EDGE_CURVE ( 'NONE', #9833, #18783, #13169, .T. ) ;
#6073=LINE ( 'NONE', #12041, #15299 ) ;
#6090=VERTEX_POINT ( 'NONE', #15473 ) ;
#6152=EDGE_CURVE ( 'NONE', #10243, #3495, #679, .T. ) ;
#6249=ORIENTED_EDGE ( 'NONE', *, *, #5939, .F. ) ;
#6289=DIRECTION ( 'NONE',  ( 0.000000000000000000, 0.000000000000000000, -1.000000000000000000 ) ) ;
#6308=TOROIDAL_SURFACE ( 'NONE', #7244, 2.200000000000001066, 0.2000000000000000111 ) ;
#6346=ORIENTED_EDGE ( 'NONE', *, *, #7937, .T. ) ;
#6358=DIRECTION ( 'NONE',  ( 0.000000000000000000, 0.000000000000000000, 1.000000000000000000 ) ) ;
#6392=ADVANCED_FACE ( 'NONE', ( #18029 ), #13600, .F. ) ;
#6396=VERTEX_POINT ( 'NONE', #16366 ) ;
#6405=CARTESIAN_POINT ( 'NONE',  ( 2.000000000000000000, -0.8865213383406694847, 1.535500000000001419 ) ) ;
#6416=ORIENTED_EDGE ( 'NONE', *, *, #18999, .T. ) ;
#6435=CARTESIAN_POINT ( 'NONE',  ( 2.000000000000000000, 0.000000000000000000, 0.000000000000000000 ) ) ;
#6509=ORIENTED_EDGE ( 'NONE', *, *, #5375, .T. ) ;
#6534=STYLED_ITEM ( 'NONE', ( #10460 ), #17389 ) ;
#6557=CARTESIAN_POINT ( 'NONE',  ( 2.000000000000000000, -0.8865213383406730374, -1.535499999999999421 ) ) ;
#6561=ADVANCED_FACE ( 'NONE', ( #12123 ), #15262, .F. ) ;
#6585=AXIS2_PLACEMENT_3D ( 'NONE', #10419, #11791, #7294 ) ;
#6603=VERTEX_POINT ( 'NONE', #15362 ) ;
#6669=CARTESIAN_POINT ( 'NONE',  ( 2.000000000000000000, -1.329782007511005837, 0.7677500000000023750 ) ) ;
#6686=ORIENTED_EDGE ( 'NONE', *, *, #11299, .T. ) ;
#6748=EDGE_CURVE ( 'NONE', #206, #15249, #2430, .T. ) ;
#6828=EDGE_LOOP ( 'NONE', ( #12442, #8763, #2919, #2727, #16425 ) ) ;
#6863=ADVANCED_FACE ( 'NONE', ( #11707 ), #6308, .F. ) ;
#6895=VERTEX_POINT ( 'NONE', #7404 ) ;
#6912=VECTOR ( 'NONE', #14362, 1000.000000000000000 ) ;
#6929=CIRCLE ( 'NONE', #4746, 1.535500000000000087 ) ;
#6966=VECTOR ( 'NONE', #5635, 1000.000000000000000 ) ;
#6976=DIRECTION ( 'NONE',  ( 0.000000000000000000, 0.4999999999999991118, -0.8660254037844390407 ) ) ;
#6989=EDGE_CURVE ( 'NONE', #8619, #4021, #3806, .T. ) ;
#7007=DIRECTION ( 'NONE',  ( -1.000000000000000000, 0.000000000000000000, -0.000000000000000000 ) ) ;
#7035=FACE_OUTER_BOUND ( 'NONE', #12081, .T. ) ;
#7046=CARTESIAN_POINT ( 'NONE',  ( 4.200000000000001954, 2.694222958124178486E-16, 2.200000000000001066 ) ) ;
#7056=AXIS2_PLACEMENT_3D ( 'NONE', #12258, #13633, #18067 ) ;
#7082=DIRECTION ( 'NONE',  ( 0.000000000000000000, 0.5000000000000011102, 0.8660254037844379305 ) ) ;
#7091=ORIENTED_EDGE ( 'NONE', *, *, #11192, .F. ) ;
#7106=ADVANCED_FACE ( 'NONE', ( #3480 ), #16815, .F. ) ;
#7111=AXIS2_PLACEMENT_3D ( 'NONE', #10765, #13712, #13892 ) ;
#7143=VERTEX_POINT ( 'NONE', #17107 ) ;
#7174=DIRECTION ( 'NONE',  ( 0.000000000000000000, -0.8660254037844391517, -0.4999999999999991673 ) ) ;
#7175=ORIENTED_EDGE ( 'NONE', *, *, #3222, .T. ) ;
#7194=DIRECTION ( 'NONE',  ( 0.000000000000000000, 0.000000000000000000, 1.000000000000000000 ) ) ;
#7202=CARTESIAN_POINT ( 'NONE',  ( 2.000000000000000000, 1.880445160090761061E-16, -1.535500000000000087 ) ) ;
#7244=AXIS2_PLACEMENT_3D ( 'NONE', #8773, #14751, #10526 ) ;
#7252=ORIENTED_EDGE ( 'NONE', *, *, #19102, .F. ) ;
#7262=CARTESIAN_POINT ( 'NONE',  ( 2.000000000000000000, 1.773042676681340524, -2.059984127722458425E-15 ) ) ;
#7277=DIRECTION ( 'NONE',  ( 1.000000000000000000, 0.000000000000000000, 0.000000000000000000 ) ) ;
#7282=EDGE_CURVE ( 'NONE', #2267, #18424, #8970, .T. ) ;
#7284=EDGE_CURVE ( 'NONE', #14560, #5728, #19351, .T. ) ;
#7285=APPLICATION_CONTEXT ( 'automotive_design' ) ;
#7294=DIRECTION ( 'NONE',  ( 0.000000000000000000, 0.000000000000000000, -1.000000000000000000 ) ) ;
#7362=LINE ( 'NONE', #5793, #17788 ) ;
#7396=DIRECTION ( 'NONE',  ( 0.000000000000000000, 0.4999999999999989453, -0.8660254037844391517 ) ) ;
#7404=CARTESIAN_POINT ( 'NONE',  ( 0.000000000000000000, 1.773042676681340524, -2.059984127722458425E-15 ) ) ;
#7409=VECTOR ( 'NONE', #2902, 1000.000000000000000 ) ;
#7421=ORIENTED_EDGE ( 'NONE', *, *, #8556, .T. ) ;
#7452=DIRECTION ( 'NONE',  ( 0.000000000000000000, 0.000000000000000000, -1.000000000000000000 ) ) ;
#7478=EDGE_CURVE ( 'NONE', #14540, #3495, #16329, .T. ) ;
#7484=DIRECTION ( 'NONE',  ( -1.000000000000000000, -0.000000000000000000, -0.000000000000000000 ) ) ;
#7502=AXIS2_PLACEMENT_3D ( 'NONE', #13150, #11675, #14913 ) ;
#7521=CARTESIAN_POINT ( 'NONE',  ( 2.000000000000000000, 1.773042676681340524, -2.059984127722458425E-15 ) ) ;
#7555=DIRECTION ( 'NONE',  ( -1.000000000000000000, -0.000000000000000000, -0.000000000000000000 ) ) ;
#7596=ORIENTED_EDGE ( 'NONE', *, *, #15767, .T. ) ;
#7724=VECTOR ( 'NONE', #10036, 1000.000000000000000 ) ;
#7774=CARTESIAN_POINT ( 'NONE',  ( 13.99999999999999822, 1.971681346627238735E-16, -1.610000000000000098 ) ) ;
#7820=EDGE_CURVE ( 'NONE', #16421, #18142, #10381, .T. ) ;
#7875=CARTESIAN_POINT ( 'NONE',  ( 2.000000000000000000, 0.000000000000000000, 0.000000000000000000 ) ) ;
#7899=CARTESIAN_POINT ( 'NONE',  ( 0.000000000000000000, 0.000000000000000000, 3.299999999999999822 ) ) ;
#7900=EDGE_CURVE ( 'NONE', #4021, #3495, #4916, .T. ) ;
#7937=EDGE_CURVE ( 'NONE', #11089, #15436, #12118, .T. ) ;
#7938=DIRECTION ( 'NONE',  ( -1.000000000000000000, -0.000000000000000000, -0.000000000000000000 ) ) ;
#8011=EDGE_LOOP ( 'NONE', ( #138, #4385, #2726, #17426 ) ) ;
#8113=ADVANCED_FACE ( 'NONE', ( #12722 ), #16822, .T. ) ;
#8232=DIRECTION ( 'NONE',  ( 0.000000000000000000, 0.000000000000000000, 1.000000000000000000 ) ) ;
#8255=CARTESIAN_POINT ( 'NONE',  ( 0.000000000000000000, -0.8865213383406694847, 1.535500000000001419 ) ) ;
#8296=LINE ( 'NONE', #14565, #15854 ) ;
#8334=DIRECTION ( 'NONE',  ( 0.000000000000000000, -1.224646799147353207E-16, 1.000000000000000000 ) ) ;
#8359=VERTEX_POINT ( 'NONE', #12025 ) ;
#8372=AXIS2_PLACEMENT_3D ( 'NONE', #15117, #7277, #4336 ) ;
#8381=CARTESIAN_POINT ( 'NONE',  ( -31.74999999999995737, 2.449293598294707893E-16, -2.000000000000000888 ) ) ;
#8386=DIRECTION ( 'NONE',  ( -1.000000000000000000, -0.000000000000000000, -0.000000000000000000 ) ) ;
#8453=LINE ( 'NONE', #14433, #18942 ) ;
#8556=EDGE_CURVE ( 'NONE', #5162, #5728, #11219, .T. ) ;
#8569=DIRECTION ( 'NONE',  ( 0.000000000000000000, 0.000000000000000000, 1.000000000000000000 ) ) ;
#8619=VERTEX_POINT ( 'NONE', #1427 ) ;
#8625=CYLINDRICAL_SURFACE ( 'NONE', #18423, 2.000000000000000888 ) ;
#8640=AXIS2_PLACEMENT_3D ( 'NONE', #3733, #17470, #8232 ) ;
#8649=PLANE ( 'NONE',  #3821 ) ;
#8763=ORIENTED_EDGE ( 'NONE', *, *, #763, .T. ) ;
#8773=CARTESIAN_POINT ( 'NONE',  ( 4.200000000000001954, 0.000000000000000000, 0.000000000000000000 ) ) ;
#8804=DIRECTION ( 'NONE',  ( 1.000000000000000000, 0.000000000000000000, 0.000000000000000000 ) ) ;
#8834=DIRECTION ( 'NONE',  ( 0.000000000000000000, 0.000000000000000000, 1.000000000000000000 ) ) ;
#8887=DIRECTION ( 'NONE',  ( 1.000000000000000000, 0.000000000000000000, 0.000000000000000000 ) ) ;
#8896=VECTOR ( 'NONE', #2396, 1000.000000000000227 ) ;
#8946=ORIENTED_EDGE ( 'NONE', *, *, #14890, .F. ) ;
#8969=CARTESIAN_POINT ( 'NONE',  ( 2.000000000000000000, 0.000000000000000000, 0.000000000000000000 ) ) ;
#8970=CIRCLE ( 'NONE', #17751, 1.610000000000000098 ) ;
#8977=MANIFOLD_SOLID_BREP ( 'Hex', #10536 ) ;
#8995=( NAMED_UNIT ( * ) PLANE_ANGLE_UNIT ( ) SI_UNIT ( $, .RADIAN. ) );
#9012=FACE_OUTER_BOUND ( 'NONE', #936, .T. ) ;
#9030=EDGE_CURVE ( 'NONE', #5728, #16469, #3847, .T. ) ;
#9035=DIRECTION ( 'NONE',  ( 1.000000000000000000, 0.000000000000000000, 0.000000000000000000 ) ) ;
#9062=VERTEX_POINT ( 'NONE', #15605 ) ;
#9095=( NAMED_UNIT ( * ) SI_UNIT ( $, .STERADIAN. ) SOLID_ANGLE_UNIT ( ) );
#9141=CIRCLE ( 'NONE', #11641, 2.000000000000000888 ) ;
#9151=VECTOR ( 'NONE', #12986, 1000.000000000000114 ) ;
#9181=CARTESIAN_POINT ( 'NONE',  ( 4.200000000000001954, 0.000000000000000000, 0.000000000000000000 ) ) ;
#9261=ORIENTED_EDGE ( 'NONE', *, *, #1001, .T. ) ;
#9284=VECTOR ( 'NONE', #3368, 1000.000000000000114 ) ;
#9324=EDGE_CURVE ( 'NONE', #18916, #206, #15825, .T. ) ;
#9445=DIRECTION ( 'NONE',  ( 0.000000000000000000, -1.000000000000000000, 1.345283343056720273E-15 ) ) ;
#9487=DIRECTION ( 'NONE',  ( -0.5000000000000061062, 0.000000000000000000, 0.8660254037844351549 ) ) ;
#9520=DIRECTION ( 'NONE',  ( 0.000000000000000000, 0.4999999999999989453, -0.8660254037844391517 ) ) ;
#9583=ORIENTED_EDGE ( 'NONE', *, *, #9324, .F. ) ;
#9585=CYLINDRICAL_SURFACE ( 'NONE', #4065, 3.500000000000000000 ) ;
#9590=ORIENTED_EDGE ( 'NONE', *, *, #19102, .T. ) ;
#9592=CARTESIAN_POINT ( 'NONE',  ( 2.000000000000000000, 1.773042676681340524, -2.059984127722458425E-15 ) ) ;
#9607=ORIENTED_EDGE ( 'NONE', *, *, #17054, .T. ) ;
#9660=EDGE_LOOP ( 'NONE', ( #15880, #5314, #7596, #18503 ) ) ;
#9681=EDGE_CURVE ( 'NONE', #440, #10132, #14395, .T. ) ;
#9709=VECTOR ( 'NONE', #7938, 1000.000000000000000 ) ;
#9767=EDGE_LOOP ( 'NONE', ( #12205, #5381, #9583, #16831 ) ) ;
#9812=CARTESIAN_POINT ( 'NONE',  ( 2.000000000000000000, 1.773042676681340524, -2.059984127722458425E-15 ) ) ;
#9820=DIRECTION ( 'NONE',  ( -1.000000000000000000, -0.000000000000000000, -0.000000000000000000 ) ) ;
#9831=LINE ( 'NONE', #15832, #14094 ) ;
#9833=VERTEX_POINT ( 'NONE', #1566 ) ;
#9859=ORIENTED_EDGE ( 'NONE', *, *, #10821, .F. ) ;
#9926=EDGE_LOOP ( 'NONE', ( #14832, #10032, #14710 ) ) ;
#9934=CARTESIAN_POINT ( 'NONE',  ( -31.74999999999995737, 0.000000000000000000, 2.000000000000000888 ) ) ;
#9959=DIRECTION ( 'NONE',  ( 0.000000000000000000, 0.000000000000000000, 1.000000000000000000 ) ) ;
#9966=CONICAL_SURFACE ( 'NONE', #13740, 1.535500000000000087, 1.047197551196590748 ) ;
#9972=ORIENTED_EDGE ( 'NONE', *, *, #14784, .F. ) ;
#9991=CARTESIAN_POINT ( 'NONE',  ( -31.74999999999995737, 0.000000000000000000, 0.000000000000000000 ) ) ;
#10019=LINE ( 'NONE', #16209, #15711 ) ;
#10032=ORIENTED_EDGE ( 'NONE', *, *, #7478, .T. ) ;
#10036=DIRECTION ( 'NONE',  ( -1.000000000000000000, -0.000000000000000000, -0.000000000000000000 ) ) ;
#10083=ORIENTED_EDGE ( 'NONE', *, *, #9030, .F. ) ;
#10111=DIRECTION ( 'NONE',  ( 0.000000000000000000, 0.5000000000000011102, 0.8660254037844379305 ) ) ;
#10114=EDGE_CURVE ( 'NONE', #4021, #14560, #8296, .T. ) ;
#10125=EDGE_LOOP ( 'NONE', ( #4905, #9972, #10707, #16727, #4178 ) ) ;
#10132=VERTEX_POINT ( 'NONE', #2643 ) ;
#10137=CARTESIAN_POINT ( 'NONE',  ( 0.000000000000000000, 1.773042676681340524, -2.059984127722458425E-15 ) ) ;
#10158=DIRECTION ( 'NONE',  ( -1.000000000000000000, -0.000000000000000000, -0.000000000000000000 ) ) ;
#10177=ORIENTED_EDGE ( 'NONE', *, *, #1001, .F. ) ;
#10243=VERTEX_POINT ( 'NONE', #16541 ) ;
#10287=DIRECTION ( 'NONE',  ( -1.000000000000000000, -0.000000000000000000, -0.000000000000000000 ) ) ;
#10301=CIRCLE ( 'NONE', #15946, 0.2000000000000000944 ) ;
#10359=AXIS2_PLACEMENT_3D ( 'NONE', #2871, #8834, #16191 ) ;
#10370=ORIENTED_EDGE ( 'NONE', *, *, #1846, .T. ) ;
#10381=LINE ( 'NONE', #14892, #15881 ) ;
#10388=FACE_OUTER_BOUND ( 'NONE', #1687, .T. ) ;
#10410=FACE_OUTER_BOUND ( 'NONE', #14046, .T. ) ;
#10419=CARTESIAN_POINT ( 'NONE',  ( 4.200000000000001954, 0.000000000000000000, -2.200000000000001066 ) ) ;
#10443=ORIENTED_EDGE ( 'NONE', *, *, #6050, .T. ) ;
#10460=PRESENTATION_STYLE_ASSIGNMENT (( #182 ) ) ;
#10468=VERTEX_POINT ( 'NONE', #15536 ) ;
#10497=DIRECTION ( 'NONE',  ( 0.000000000000000000, 0.000000000000000000, 1.000000000000000000 ) ) ;
#10510=CARTESIAN_POINT ( 'NONE',  ( 0.1999999999999987899, 0.000000000000000000, 0.000000000000000000 ) ) ;
#10518=FACE_BOUND ( 'NONE', #2043, .T. ) ;
#10526=DIRECTION ( 'NONE',  ( 0.000000000000000000, 0.000000000000000000, -1.000000000000000000 ) ) ;
#10536=CLOSED_SHELL ( 'NONE', ( #13973, #2570, #1494, #16097, #5871, #14679, #789, #14706, #3335, #1757, #10832, #2215, #6863, #8113, #12382, #7106, #2594, #2241, #6561, #12360, #3174, #6392, #18173, #1746, #5914, #2655, #13926 ) ) ;
#10537=ORIENTED_EDGE ( 'NONE', *, *, #5478, .T. ) ;
#10550=SHAPE_REPRESENTATION ( 'socket head cap screw_iso_ISO 4762 M4 x 10 - 10N', ( #10359 ), #4043 ) ;
#10556=( NAMED_UNIT ( * ) SI_UNIT ( $, .STERADIAN. ) SOLID_ANGLE_UNIT ( ) );
#10560=ORIENTED_EDGE ( 'NONE', *, *, #3546, .T. ) ;
#10642=ORIENTED_EDGE ( 'NONE', *, *, #12215, .F. ) ;
#10658=FILL_AREA_STYLE_COLOUR ( '', #14997 ) ;
#10662=VECTOR ( 'NONE', #4713, 1000.000000000000000 ) ;
#10696=CARTESIAN_POINT ( 'NONE',  ( 4.200000000000001954, 0.000000000000000000, 0.000000000000000000 ) ) ;
#10707=ORIENTED_EDGE ( 'NONE', *, *, #5375, .F. ) ;
#10749=EDGE_CURVE ( 'NONE', #16421, #10468, #9831, .T. ) ;
#10765=CARTESIAN_POINT ( 'NONE',  ( 4.000000000000000000, 0.000000000000000000, 0.000000000000000000 ) ) ;
#10778=DIRECTION ( 'NONE',  ( -1.000000000000000000, -0.000000000000000000, -0.000000000000000000 ) ) ;
#10821=EDGE_CURVE ( 'NONE', #15249, #15436, #15369, .T. ) ;
#10832=ADVANCED_FACE ( 'NONE', ( #2797 ), #1917, .T. ) ;
#10938=EDGE_LOOP ( 'NONE', ( #7252, #10370, #6686, #2317 ) ) ;
#10965=AXIS2_PLACEMENT_3D ( 'NONE', #12630, #17062, #3524 ) ;
#10967=ORIENTED_EDGE ( 'NONE', *, *, #10114, .F. ) ;
#11018=ORIENTED_EDGE ( 'NONE', *, *, #13922, .F. ) ;
#11089=VERTEX_POINT ( 'NONE', #2145 ) ;
#11131=CARTESIAN_POINT ( 'NONE',  ( 2.000000000000000000, 0.000000000000000000, 0.000000000000000000 ) ) ;
#11181=CARTESIAN_POINT ( 'NONE',  ( 13.99999999999999822, 0.000000000000000000, 1.610000000000000098 ) ) ;
#11192=EDGE_CURVE ( 'NONE', #6090, #10132, #6929, .T. ) ;
#11219=LINE ( 'NONE', #17225, #17473 ) ;
#11247=DIRECTION ( 'NONE',  ( 0.000000000000000000, -0.4999999999999989453, 0.8660254037844391517 ) ) ;
#11253=CIRCLE ( 'NONE', #7502, 3.500000000000000000 ) ;
#11272=VECTOR ( 'NONE', #13260, 1000.000000000000000 ) ;
#11280=DIRECTION ( 'NONE',  ( -0.7071067811865350272, 0.000000000000000000, 0.7071067811865598962 ) ) ;
#11299=EDGE_CURVE ( 'NONE', #9833, #6603, #13107, .T. ) ;
#11340=CARTESIAN_POINT ( 'NONE',  ( 2.000000000000000000, 0.000000000000000000, 0.000000000000000000 ) ) ;
#11351=EDGE_CURVE ( 'NONE', #5162, #16099, #13588, .T. ) ;
#11366=DIRECTION ( 'NONE',  ( -1.000000000000000000, -0.000000000000000000, -0.000000000000000000 ) ) ;
#11426=CARTESIAN_POINT ( 'NONE',  ( 0.000000000000000000, 0.8865213383406680414, -1.535500000000000975 ) ) ;
#11464=CARTESIAN_POINT ( 'NONE',  ( 2.000000000000000000, 1.773042676681340524, -2.059984127722458425E-15 ) ) ;
#11502=EDGE_LOOP ( 'NONE', ( #13601, #10967, #5053 ) ) ;
#11550=CONICAL_SURFACE ( 'NONE', #5609, 1.610000000000000098, 0.7853981633974658205 ) ;
#11559=FACE_OUTER_BOUND ( 'NONE', #5264, .T. ) ;
#11566=DIRECTION ( 'NONE',  ( 0.000000000000000000, 0.000000000000000000, -1.000000000000000000 ) ) ;
#11611=PLANE ( 'NONE',  #5084 ) ;
#11641=AXIS2_PLACEMENT_3D ( 'NONE', #9181, #8887, #4686 ) ;
#11675=DIRECTION ( 'NONE',  ( 1.000000000000000000, 0.000000000000000000, 0.000000000000000000 ) ) ;
#11678=EDGE_CURVE ( 'NONE', #18916, #6396, #17412, .T. ) ;
#11707=FACE_OUTER_BOUND ( 'NONE', #2038, .T. ) ;
#11722=ORIENTED_EDGE ( 'NONE', *, *, #11678, .F. ) ;
#11791=DIRECTION ( 'NONE',  ( 0.000000000000000000, -1.000000000000000000, 0.000000000000000000 ) ) ;
#11807=AXIS2_PLACEMENT_3D ( 'NONE', #2295, #7174, #6976 ) ;
#11814=ORIENTED_EDGE ( 'NONE', *, *, #1388, .T. ) ;
#11824=ORIENTED_EDGE ( 'NONE', *, *, #12996, .T. ) ;
#11858=CARTESIAN_POINT ( 'NONE',  ( 13.99999999999999822, 0.000000000000000000, 0.000000000000000000 ) ) ;
#11862=ORIENTED_EDGE ( 'NONE', *, *, #6748, .T. ) ;
#11941=( LENGTH_UNIT ( ) NAMED_UNIT ( * ) SI_UNIT ( .MILLI., .METRE. ) );
#11944=AXIS2_PLACEMENT_3D ( 'NONE', #2504, #9820, #13258 ) ;
#11987=FACE_OUTER_BOUND ( 'NONE', #9767, .T. ) ;
#12004=ORIENTED_EDGE ( 'NONE', *, *, #2978, .T. ) ;
#12025=CARTESIAN_POINT ( 'NONE',  ( 0.1999999999999987899, 4.286263797015736595E-16, -3.500000000000000000 ) ) ;
#12041=CARTESIAN_POINT ( 'NONE',  ( 2.000000000000000000, 1.773042676681340524, -2.059984127722458425E-15 ) ) ;
#12076=CARTESIAN_POINT ( 'NONE',  ( 2.000000000000000000, 1.773042676681340524, -2.059984127722458425E-15 ) ) ;
#12081=EDGE_LOOP ( 'NONE', ( #2314, #12460 ) ) ;
#12118=CIRCLE ( 'NONE', #7111, 2.200000000000001066 ) ;
#12123=FACE_OUTER_BOUND ( 'NONE', #10125, .T. ) ;
#12150=CARTESIAN_POINT ( 'NONE',  ( -31.74999999999995737, 0.000000000000000000, 0.000000000000000000 ) ) ;
#12153=DIRECTION ( 'NONE',  ( -1.000000000000000000, -0.000000000000000000, -0.000000000000000000 ) ) ;
#12155=ORIENTED_EDGE ( 'NONE', *, *, #14890, .T. ) ;
#12168=CARTESIAN_POINT ( 'NONE',  ( 13.99999999999999822, 0.000000000000000000, 0.000000000000000000 ) ) ;
#12205=ORIENTED_EDGE ( 'NONE', *, *, #7282, .T. ) ;
#12215=EDGE_CURVE ( 'NONE', #18424, #206, #16804, .T. ) ;
#12219=AXIS2_PLACEMENT_3D ( 'NONE', #16265, #8804, #1357 ) ;
#12258=CARTESIAN_POINT ( 'NONE',  ( 13.61000000000001009, 0.000000000000000000, 0.000000000000000000 ) ) ;
#12306=ORIENTED_EDGE ( 'NONE', *, *, #3544, .F. ) ;
#12360=ADVANCED_FACE ( 'NONE', ( #17593 ), #3751, .F. ) ;
#12375=DIRECTION ( 'NONE',  ( 0.000000000000000000, -0.4999999999999991118, 0.8660254037844391517 ) ) ;
#12382=ADVANCED_FACE ( 'NONE', ( #2493 ), #15715, .T. ) ;
#12385=DIRECTION ( 'NONE',  ( 0.000000000000000000, 0.000000000000000000, 1.000000000000000000 ) ) ;
#12388=AXIS2_PLACEMENT_3D ( 'NONE', #16071, #769, #11247 ) ;
#12442=ORIENTED_EDGE ( 'NONE', *, *, #6152, .F. ) ;
#12446=AXIS2_PLACEMENT_3D ( 'NONE', #12168, #3172, #10497 ) ;
#12460=ORIENTED_EDGE ( 'NONE', *, *, #1388, .F. ) ;
#12501=VECTOR ( 'NONE', #11280, 1000.000000000000114 ) ;
#12512=AXIS2_PLACEMENT_3D ( 'NONE', #11464, #5595, #11566 ) ;
#12542=DIRECTION ( 'NONE',  ( 0.000000000000000000, 0.000000000000000000, 1.000000000000000000 ) ) ;
#12585=ORIENTED_EDGE ( 'NONE', *, *, #819, .F. ) ;
#12609=ORIENTED_EDGE ( 'NONE', *, *, #2592, .T. ) ;
#12630=CARTESIAN_POINT ( 'NONE',  ( 4.000000000000003553, 0.000000000000000000, 0.000000000000000000 ) ) ;
#12691=ORIENTED_EDGE ( 'NONE', *, *, #3794, .T. ) ;
#12722=FACE_OUTER_BOUND ( 'NONE', #9660, .T. ) ;
#12760=CARTESIAN_POINT ( 'NONE',  ( 0.000000000000000000, -1.773042676681341856, 2.276824562219559311E-15 ) ) ;
#12785=ORIENTED_EDGE ( 'NONE', *, *, #11351, .F. ) ;
#12809=CARTESIAN_POINT ( 'NONE',  ( 2.000000000000000000, 0.000000000000000000, 0.000000000000000000 ) ) ;
#12828=FACE_OUTER_BOUND ( 'NONE', #17249, .T. ) ;
#12832=ORIENTED_EDGE ( 'NONE', *, *, #11299, .F. ) ;
#12852=LINE ( 'NONE', #604, #15056 ) ;
#12859=LINE ( 'NONE', #11181, #12501 ) ;
#12880=AXIS2_PLACEMENT_3D ( 'NONE', #7262, #18055, #7452 ) ;
#12898=DIRECTION ( 'NONE',  ( -0.000000000000000000, 0.000000000000000000, 1.000000000000000000 ) ) ;
#12907=DIRECTION ( 'NONE',  ( 0.000000000000000000, -1.000000000000000000, 9.783878858594328898E-16 ) ) ;
#12916=ORIENTED_EDGE ( 'NONE', *, *, #3413, .T. ) ;
#12918=DIRECTION ( 'NONE',  ( 0.000000000000000000, 0.000000000000000000, 1.000000000000000000 ) ) ;
#12923=PLANE ( 'NONE',  #12388 ) ;
#12942=CARTESIAN_POINT ( 'NONE',  ( 0.000000000000000000, -1.773042676681341856, 2.276824562219559311E-15 ) ) ;
#12957=DIRECTION ( 'NONE',  ( 0.000000000000000000, -0.5000000000000011102, -0.8660254037844379305 ) ) ;
#12971=DIRECTION ( 'NONE',  ( -1.000000000000000000, -0.000000000000000000, -0.000000000000000000 ) ) ;
#12986=DIRECTION ( 'NONE',  ( 0.000000000000000000, -0.5000000000000011102, -0.8660254037844379305 ) ) ;
#12987=EDGE_CURVE ( 'NONE', #8359, #4627, #16852, .T. ) ;
#12995=ORIENTED_EDGE ( 'NONE', *, *, #17190, .T. ) ;
#12996=EDGE_CURVE ( 'NONE', #14540, #5162, #7362, .T. ) ;
#13039=CARTESIAN_POINT ( 'NONE',  ( 2.000000000000000000, 1.773042676681340524, -2.059984127722458425E-15 ) ) ;
#13060=CARTESIAN_POINT ( 'NONE',  ( 2.000000000000000000, -1.773042676681341856, 2.276824562219559311E-15 ) ) ;
#13107=LINE ( 'NONE', #18824, #2575 ) ;
#13150=CARTESIAN_POINT ( 'NONE',  ( 0.1999999999999987899, 0.000000000000000000, 0.000000000000000000 ) ) ;
#13169=CIRCLE ( 'NONE', #10965, 3.500000000000000000 ) ;
#13170=AXIS2_PLACEMENT_3D ( 'NONE', #13367, #7484, #7194 ) ;
#13253=DIRECTION ( 'NONE',  ( 0.000000000000000000, 0.000000000000000000, -1.000000000000000000 ) ) ;
#13258=DIRECTION ( 'NONE',  ( 0.000000000000000000, 0.000000000000000000, 1.000000000000000000 ) ) ;
#13260=DIRECTION ( 'NONE',  ( -1.000000000000000000, -0.000000000000000000, -0.000000000000000000 ) ) ;
#13367=CARTESIAN_POINT ( 'NONE',  ( 13.99999999999999822, 0.000000000000000000, 0.000000000000000000 ) ) ;
#13436=FACE_OUTER_BOUND ( 'NONE', #9926, .T. ) ;
#13445=CARTESIAN_POINT ( 'NONE',  ( 0.000000000000000000, -0.8865213383406730374, -1.535499999999999421 ) ) ;
#13517=( LENGTH_UNIT ( ) NAMED_UNIT ( * ) SI_UNIT ( .MILLI., .METRE. ) );
#13568=CARTESIAN_POINT ( 'NONE',  ( 2.000000000000000000, 2.065682573263594481E-15, 1.535500000000000309 ) ) ;
#13588=LINE ( 'NONE', #3215, #5363 ) ;
#13600=PLANE ( 'NONE',  #12219 ) ;
#13601=ORIENTED_EDGE ( 'NONE', *, *, #3413, .F. ) ;
#13633=DIRECTION ( 'NONE',  ( -1.000000000000000000, -0.000000000000000000, -0.000000000000000000 ) ) ;
#13694=CIRCLE ( 'NONE', #12446, 1.610000000000000098 ) ;
#13696=DIRECTION ( 'NONE',  ( -1.000000000000000000, -0.000000000000000000, -0.000000000000000000 ) ) ;
#13712=DIRECTION ( 'NONE',  ( -1.000000000000000000, -0.000000000000000000, -0.000000000000000000 ) ) ;
#13736=CARTESIAN_POINT ( 'NONE',  ( 2.000000000000000000, 0.8865213383406680414, -1.535500000000000975 ) ) ;
#13740=AXIS2_PLACEMENT_3D ( 'NONE', #11131, #18618, #18811 ) ;
#13748=CIRCLE ( 'NONE', #17848, 3.500000000000000000 ) ;
#13754=LINE ( 'NONE', #5030, #18309 ) ;
#13766=ORIENTED_EDGE ( 'NONE', *, *, #1846, .F. ) ;
#13805=EDGE_CURVE ( 'NONE', #3495, #6090, #897, .T. ) ;
#13858=ORIENTED_EDGE ( 'NONE', *, *, #9030, .T. ) ;
#13892=DIRECTION ( 'NONE',  ( 0.000000000000000000, 0.000000000000000000, -1.000000000000000000 ) ) ;
#13910=LINE ( 'NONE', #9592, #9709 ) ;
#13922=EDGE_CURVE ( 'NONE', #18142, #16469, #15759, .T. ) ;
#13926=ADVANCED_FACE ( 'NONE', ( #2244 ), #1859, .F. ) ;
#13973=ADVANCED_FACE ( 'NONE', ( #850 ), #9966, .F. ) ;
#13991=CIRCLE ( 'NONE', #8372, 2.000000000000000888 ) ;
#14046=EDGE_LOOP ( 'NONE', ( #15604, #18604, #15373 ) ) ;
#14071=EDGE_CURVE ( 'NONE', #10468, #8619, #3111, .T. ) ;
#14077=EDGE_LOOP ( 'NONE', ( #15225, #12785, #7421, #13858, #11018, #12585 ) ) ;
#14094=VECTOR ( 'NONE', #18892, 1000.000000000000000 ) ;
#14123=( LENGTH_UNIT ( ) NAMED_UNIT ( * ) SI_UNIT ( .MILLI., .METRE. ) );
#14140=CARTESIAN_POINT ( 'NONE',  ( 4.000000000000003553, 4.286263797015736595E-16, -3.500000000000000000 ) ) ;
#14362=DIRECTION ( 'NONE',  ( -1.000000000000000000, -0.000000000000000000, -0.000000000000000000 ) ) ;
#14385=PLANE ( 'NONE',  #4570 ) ;
#14395=LINE ( 'NONE', #4017, #17416 ) ;
#14433=CARTESIAN_POINT ( 'NONE',  ( 2.000000000000000000, -0.8865213383406694847, 1.535500000000001419 ) ) ;
#14540=VERTEX_POINT ( 'NONE', #4720 ) ;
#14545=DIRECTION ( 'NONE',  ( -1.000000000000000000, -0.000000000000000000, -0.000000000000000000 ) ) ;
#14547=CARTESIAN_POINT ( 'NONE',  ( 0.000000000000000000, 0.000000000000000000, 0.000000000000000000 ) ) ;
#14560=VERTEX_POINT ( 'NONE', #5917 ) ;
#14565=CARTESIAN_POINT ( 'NONE',  ( 2.000000000000000000, -0.8865213383406694847, 1.535500000000001419 ) ) ;
#14582=ORIENTED_EDGE ( 'NONE', *, *, #16258, .T. ) ;
#14598=DIRECTION ( 'NONE',  ( 0.000000000000000000, 0.000000000000000000, 1.000000000000000000 ) ) ;
#14603=CARTESIAN_POINT ( 'NONE',  ( 0.000000000000000000, 0.8865213383406680414, -1.535500000000000975 ) ) ;
#14639=PRODUCT_DEFINITION ( 'UNKNOWN', '', #17648, #17956 ) ;
#14679=ADVANCED_FACE ( 'NONE', ( #1775 ), #5622, .T. ) ;
#14706=ADVANCED_FACE ( 'NONE', ( #4814 ), #9585, .T. ) ;
#14710=ORIENTED_EDGE ( 'NONE', *, *, #7900, .F. ) ;
#14723=CIRCLE ( 'NONE', #19158, 3.299999999999999822 ) ;
#14751=DIRECTION ( 'NONE',  ( 1.000000000000000000, 0.000000000000000000, 0.000000000000000000 ) ) ;
#14766=DIRECTION ( 'NONE',  ( -1.000000000000000000, -0.000000000000000000, -0.000000000000000000 ) ) ;
#14784=EDGE_CURVE ( 'NONE', #9062, #16469, #3623, .T. ) ;
#14832=ORIENTED_EDGE ( 'NONE', *, *, #3794, .F. ) ;
#14859=CARTESIAN_POINT ( 'NONE',  ( 4.000000000000001776, 0.000000000000000000, -2.200000000000001066 ) ) ;
#14890=EDGE_CURVE ( 'NONE', #6396, #11089, #19392, .T. ) ;
#14892=CARTESIAN_POINT ( 'NONE',  ( 2.000000000000000000, 0.8865213383406680414, -1.535500000000000975 ) ) ;
#14913=DIRECTION ( 'NONE',  ( 0.000000000000000000, 0.000000000000000000, 1.000000000000000000 ) ) ;
#14927=CARTESIAN_POINT ( 'NONE',  ( 0.000000000000000000, 0.000000000000000000, 0.000000000000000000 ) ) ;
#14940=DIRECTION ( 'NONE',  ( 0.000000000000000000, 0.000000000000000000, -1.000000000000000000 ) ) ;
#14974=AXIS2_PLACEMENT_3D ( 'NONE', #7046, #4207, #17458 ) ;
#14976=ORIENTED_EDGE ( 'NONE', *, *, #819, .T. ) ;
#14997=COLOUR_RGB ( '',1.000000000000000000, 0.9490196078431372140, 0.9098039215686274384 ) ;
#15017=VECTOR ( 'NONE', #10778, 1000.000000000000000 ) ;
#15056=VECTOR ( 'NONE', #17180, 1000.000000000000000 ) ;
#15081=EDGE_CURVE ( 'NONE', #10132, #16421, #6073, .T. ) ;
#15114=CARTESIAN_POINT ( 'NONE',  ( 4.000000000000000000, 0.000000000000000000, 0.000000000000000000 ) ) ;
#15117=CARTESIAN_POINT ( 'NONE',  ( 4.200000000000001954, 0.000000000000000000, 0.000000000000000000 ) ) ;
#15225=ORIENTED_EDGE ( 'NONE', *, *, #3544, .T. ) ;
#15241=ORIENTED_EDGE ( 'NONE', *, *, #1392, .F. ) ;
#15249=VERTEX_POINT ( 'NONE', #3512 ) ;
#15262=PLANE ( 'NONE',  #17260 ) ;
#15299=VECTOR ( 'NONE', #16375, 1000.000000000000114 ) ;
#15362=CARTESIAN_POINT ( 'NONE',  ( 0.1999999999999987899, 0.000000000000000000, 3.500000000000000000 ) ) ;
#15369=CIRCLE ( 'NONE', #6585, 0.2000000000000000944 ) ;
#15373=ORIENTED_EDGE ( 'NONE', *, *, #3546, .F. ) ;
#15418=ORIENTED_EDGE ( 'NONE', *, *, #10114, .T. ) ;
#15436=VERTEX_POINT ( 'NONE', #14859 ) ;
#15471=AXIS2_PLACEMENT_3D ( 'NONE', #7875, #2001, #18384 ) ;
#15473=CARTESIAN_POINT ( 'NONE',  ( 2.000000000000000000, 1.329782007511006281, 0.7677499999999984892 ) ) ;
#15536=CARTESIAN_POINT ( 'NONE',  ( 2.000000000000000000, -1.502314598737159426E-15, -1.535500000000000087 ) ) ;
#15604=ORIENTED_EDGE ( 'NONE', *, *, #15081, .T. ) ;
#15605=CARTESIAN_POINT ( 'NONE',  ( 2.000000000000000000, -0.8865213383406730374, -1.535499999999999421 ) ) ;
#15662=EDGE_LOOP ( 'NONE', ( #6509, #17184, #17693 ) ) ;
#15676=DIRECTION ( 'NONE',  ( 0.000000000000000000, 0.000000000000000000, -1.000000000000000000 ) ) ;
#15711=VECTOR ( 'NONE', #19178, 1000.000000000000000 ) ;
#15715=PLANE ( 'NONE',  #11807 ) ;
#15730=EDGE_LOOP ( 'NONE', ( #17504, #12155, #581, #9859 ) ) ;
#15743=DIRECTION ( 'NONE',  ( 0.000000000000000000, 0.000000000000000000, -1.000000000000000000 ) ) ;
#15747=DIRECTION ( 'NONE',  ( 0.000000000000000000, -0.5000000000000011102, -0.8660254037844379305 ) ) ;
#15759=LINE ( 'NONE', #11426, #16882 ) ;
#15767=EDGE_CURVE ( 'NONE', #6603, #3135, #10301, .T. ) ;
#15780=ORIENTED_EDGE ( 'NONE', *, *, #7284, .F. ) ;
#15799=CARTESIAN_POINT ( 'NONE',  ( 0.1999999999999987899, 4.041334437186265510E-16, -3.299999999999999822 ) ) ;
#15825=CIRCLE ( 'NONE', #7056, 2.000000000000001332 ) ;
#15832=CARTESIAN_POINT ( 'NONE',  ( 2.000000000000000000, 0.8865213383406680414, -1.535500000000000975 ) ) ;
#15854=VECTOR ( 'NONE', #15859, 1000.000000000000114 ) ;
#15859=DIRECTION ( 'NONE',  ( 0.000000000000000000, -0.5000000000000011102, -0.8660254037844379305 ) ) ;
#15880=ORIENTED_EDGE ( 'NONE', *, *, #12987, .F. ) ;
#15881=VECTOR ( 'NONE', #3853, 1000.000000000000000 ) ;
#15892=DIRECTION ( 'NONE',  ( 1.000000000000000000, 0.000000000000000000, 0.000000000000000000 ) ) ;
#15946=AXIS2_PLACEMENT_3D ( 'NONE', #18113, #4675, #16641 ) ;
#15952=ORIENTED_EDGE ( 'NONE', *, *, #15996, .T. ) ;
#15996=EDGE_CURVE ( 'NONE', #8359, #6603, #13748, .T. ) ;
#16027=TOROIDAL_SURFACE ( 'NONE', #11944, 3.299999999999999822, 0.2000000000000000111 ) ;
#16037=ORIENTED_EDGE ( 'NONE', *, *, #6152, .T. ) ;
#16071=CARTESIAN_POINT ( 'NONE',  ( 2.000000000000000000, -1.773042676681341856, 2.276824562219559311E-15 ) ) ;
#16097=ADVANCED_FACE ( 'NONE', ( #11987 ), #11550, .T. ) ;
#16098=SHAPE_DEFINITION_REPRESENTATION ( #5707, #10550 ) ;
#16099=VERTEX_POINT ( 'NONE', #2896 ) ;
#16102=AXIS2_PLACEMENT_3D ( 'NONE', #4464, #4657, #14940 ) ;
#16126=DIRECTION ( 'NONE',  ( -1.000000000000000000, -0.000000000000000000, -0.000000000000000000 ) ) ;
#16177=ORIENTED_EDGE ( 'NONE', *, *, #3759, .T. ) ;
#16191=DIRECTION ( 'NONE',  ( 1.000000000000000000, 0.000000000000000000, 0.000000000000000000 ) ) ;
#16203=LINE ( 'NONE', #13060, #8896 ) ;
#16209=CARTESIAN_POINT ( 'NONE',  ( 2.000000000000000000, -0.8865213383406694847, 1.535500000000001419 ) ) ;
#16230=AXIS2_PLACEMENT_3D ( 'NONE', #15799, #2380, #8334 ) ;
#16232=FACE_OUTER_BOUND ( 'NONE', #19411, .T. ) ;
#16242=DIRECTION ( 'NONE',  ( -1.000000000000000000, -0.000000000000000000, -0.000000000000000000 ) ) ;
#16258=EDGE_CURVE ( 'NONE', #2267, #18916, #12859, .T. ) ;
#16264=CARTESIAN_POINT ( 'NONE',  ( 13.99999999999999822, 0.000000000000000000, 1.610000000000000098 ) ) ;
#16265=CARTESIAN_POINT ( 'NONE',  ( 2.000000000000000000, 1.773042676681340524, -2.059984127722458425E-15 ) ) ;
#16329=LINE ( 'NONE', #19391, #7409 ) ;
#16366=CARTESIAN_POINT ( 'NONE',  ( 4.200000000000001954, 0.000000000000000000, 2.000000000000000888 ) ) ;
#16375=DIRECTION ( 'NONE',  ( 0.000000000000000000, -0.5000000000000011102, -0.8660254037844379305 ) ) ;
#16389=CYLINDRICAL_SURFACE ( 'NONE', #17908, 2.000000000000000888 ) ;
#16421=VERTEX_POINT ( 'NONE', #17874 ) ;
#16425=ORIENTED_EDGE ( 'NONE', *, *, #7900, .T. ) ;
#16438=ORIENTED_EDGE ( 'NONE', *, *, #8556, .F. ) ;
#16458=EDGE_CURVE ( 'NONE', #6603, #8359, #11253, .T. ) ;
#16469=VERTEX_POINT ( 'NONE', #13445 ) ;
#16503=LINE ( 'NONE', #13736, #5132 ) ;
#16522=CARTESIAN_POINT ( 'NONE',  ( 2.000000000000000000, -1.773042676681341856, 2.276824562219559311E-15 ) ) ;
#16530=AXIS2_PLACEMENT_3D ( 'NONE', #9812, #1013, #10111 ) ;
#16541=CARTESIAN_POINT ( 'NONE',  ( 2.886521338340684917, 0.000000000000000000, 0.000000000000000000 ) ) ;
#16546=DIRECTION ( 'NONE',  ( 0.000000000000000000, 1.000000000000000000, -1.345283343056720273E-15 ) ) ;
#16579=LINE ( 'NONE', #201, #10662 ) ;
#16600=DIRECTION ( 'NONE',  ( 1.000000000000000000, 0.000000000000000000, 0.000000000000000000 ) ) ;
#16602=DIRECTION ( 'NONE',  ( -1.000000000000000000, -0.000000000000000000, -0.000000000000000000 ) ) ;
#16641=DIRECTION ( 'NONE',  ( 0.000000000000000000, 0.000000000000000000, -1.000000000000000000 ) ) ;
#16658=DIRECTION ( 'NONE',  ( 0.000000000000000000, -9.783878858594328898E-16, -1.000000000000000000 ) ) ;
#16664=DIRECTION ( 'NONE',  ( 0.000000000000000000, 0.000000000000000000, 1.000000000000000000 ) ) ;
#16665=FILL_AREA_STYLE ('',( #10658 ) ) ;
#16671=ORIENTED_EDGE ( 'NONE', *, *, #7284, .T. ) ;
#16694=CARTESIAN_POINT ( 'NONE',  ( 13.61000000000001009, 2.449293598294708386E-16, -2.000000000000001332 ) ) ;
#16698=DIRECTION ( 'NONE',  ( 0.000000000000000000, -1.000000000000000000, 9.783878858594328898E-16 ) ) ;
#16727=ORIENTED_EDGE ( 'NONE', *, *, #10749, .F. ) ;
#16764=CARTESIAN_POINT ( 'NONE',  ( 2.000000000000000000, 0.000000000000000000, 0.000000000000000000 ) ) ;
#16804=LINE ( 'NONE', #7774, #9284 ) ;
#16815=PLANE ( 'NONE',  #367 ) ;
#16822=TOROIDAL_SURFACE ( 'NONE', #3671, 3.299999999999999822, 0.2000000000000000111 ) ;
#16831=ORIENTED_EDGE ( 'NONE', *, *, #16258, .F. ) ;
#16852=CIRCLE ( 'NONE', #16230, 0.2000000000000000944 ) ;
#16882=VECTOR ( 'NONE', #12907, 1000.000000000000000 ) ;
#16916=DIRECTION ( 'NONE',  ( -0.000000000000000000, 1.345283343056720273E-15, 1.000000000000000000 ) ) ;
#16930=ORIENTED_EDGE ( 'NONE', *, *, #9681, .T. ) ;
#16971=AXIS2_PLACEMENT_3D ( 'NONE', #4338, #16602, #217 ) ;
#17044=CIRCLE ( 'NONE', #2008, 2.000000000000001332 ) ;
#17054=EDGE_CURVE ( 'NONE', #15436, #11089, #18821, .T. ) ;
#17062=DIRECTION ( 'NONE',  ( -1.000000000000000000, -0.000000000000000000, -0.000000000000000000 ) ) ;
#17080=MECHANICAL_DESIGN_GEOMETRIC_PRESENTATION_REPRESENTATION('',(#4853),#3920);
#17107=CARTESIAN_POINT ( 'NONE',  ( 2.000000000000000000, 0.8865213383406715941, 1.535499999999999199 ) ) ;
#17180=DIRECTION ( 'NONE',  ( 0.000000000000000000, -0.4999999999999991118, 0.8660254037844391517 ) ) ;
#17184=ORIENTED_EDGE ( 'NONE', *, *, #3759, .F. ) ;
#17190=EDGE_CURVE ( 'NONE', #440, #6895, #13910, .T. ) ;
#17222=CARTESIAN_POINT ( 'NONE',  ( 2.000000000000000000, 1.773042676681340524, -2.059984127722458425E-15 ) ) ;
#17225=CARTESIAN_POINT ( 'NONE',  ( 0.000000000000000000, -0.8865213383406694847, 1.535500000000001419 ) ) ;
#17249=EDGE_LOOP ( 'NONE', ( #10083, #15780, #12916, #16177, #18908 ) ) ;
#17260=AXIS2_PLACEMENT_3D ( 'NONE', #18322, #16658, #4878 ) ;
#17277=DIRECTION ( 'NONE',  ( 0.000000000000000000, 0.000000000000000000, -1.000000000000000000 ) ) ;
#17288=( NAMED_UNIT ( * ) SI_UNIT ( $, .STERADIAN. ) SOLID_ANGLE_UNIT ( ) );
#17353=CARTESIAN_POINT ( 'NONE',  ( 14.00000000000000000, 1.610000000000000098, 0.000000000000000000 ) ) ;
#17389=ADVANCED_BREP_SHAPE_REPRESENTATION ( '', ( #8977, #10359 ), #4043 ) ;
#17412=LINE ( 'NONE', #9934, #7724 ) ;
#17416=VECTOR ( 'NONE', #17560, 1000.000000000000114 ) ;
#17426=ORIENTED_EDGE ( 'NONE', *, *, #15767, .F. ) ;
#17458=DIRECTION ( 'NONE',  ( 0.000000000000000000, 1.224646799147353207E-16, 1.000000000000000000 ) ) ;
#17470=DIRECTION ( 'NONE',  ( -1.000000000000000000, -0.000000000000000000, -0.000000000000000000 ) ) ;
#17473=VECTOR ( 'NONE', #15747, 1000.000000000000114 ) ;
#17504=ORIENTED_EDGE ( 'NONE', *, *, #2978, .F. ) ;
#17519=MECHANICAL_DESIGN_GEOMETRIC_PRESENTATION_REPRESENTATION('',(#6534),#5278);
#17560=DIRECTION ( 'NONE',  ( 0.000000000000000000, -0.5000000000000011102, -0.8660254037844379305 ) ) ;
#17593=FACE_OUTER_BOUND ( 'NONE', #5756, .T. ) ;
#17603=CIRCLE ( 'NONE', #16971, 3.299999999999999822 ) ;
#17648=PRODUCT_DEFINITION_FORMATION_WITH_SPECIFIED_SOURCE ( 'ANY', '', #4297, .NOT_KNOWN. ) ;
#17658=ORIENTED_EDGE ( 'NONE', *, *, #2592, .F. ) ;
#17693=ORIENTED_EDGE ( 'NONE', *, *, #14071, .F. ) ;
#17749=ORIENTED_EDGE ( 'NONE', *, *, #15081, .F. ) ;
#17751=AXIS2_PLACEMENT_3D ( 'NONE', #11858, #7555, #4620 ) ;
#17785=LINE ( 'NONE', #6020, #11272 ) ;
#17788=VECTOR ( 'NONE', #1685, 1000.000000000000000 ) ;
#17795=DIRECTION ( 'NONE',  ( 1.000000000000000000, 0.000000000000000000, 0.000000000000000000 ) ) ;
#17848=AXIS2_PLACEMENT_3D ( 'NONE', #10510, #17795, #8569 ) ;
#17874=CARTESIAN_POINT ( 'NONE',  ( 2.000000000000000000, 0.8865213383406680414, -1.535500000000000975 ) ) ;
#17896=DIRECTION ( 'NONE',  ( 0.000000000000000000, 0.000000000000000000, 1.000000000000000000 ) ) ;
#17908=AXIS2_PLACEMENT_3D ( 'NONE', #12150, #10287, #19246 ) ;
#17945=ORIENTED_EDGE ( 'NONE', *, *, #3222, .F. ) ;
#17956=PRODUCT_DEFINITION_CONTEXT ( 'detailed design', #7285, 'design' ) ;
#18029=FACE_OUTER_BOUND ( 'NONE', #11502, .T. ) ;
#18055=DIRECTION ( 'NONE',  ( 1.000000000000000000, 0.000000000000000000, 0.000000000000000000 ) ) ;
#18067=DIRECTION ( 'NONE',  ( 0.000000000000000000, 0.000000000000000000, 1.000000000000000000 ) ) ;
#18113=CARTESIAN_POINT ( 'NONE',  ( 0.1999999999999987899, 0.000000000000000000, 3.299999999999999822 ) ) ;
#18142=VERTEX_POINT ( 'NONE', #14603 ) ;
#18173=ADVANCED_FACE ( 'NONE', ( #13436 ), #5494, .F. ) ;
#18259=DIRECTION ( 'NONE',  ( -1.000000000000000000, -0.000000000000000000, -0.000000000000000000 ) ) ;
#18309=VECTOR ( 'NONE', #12375, 1000.000000000000000 ) ;
#18322=CARTESIAN_POINT ( 'NONE',  ( 2.000000000000000000, 0.8865213383406680414, -1.535500000000000975 ) ) ;
#18328=( NAMED_UNIT ( * ) PLANE_ANGLE_UNIT ( ) SI_UNIT ( $, .RADIAN. ) );
#18384=DIRECTION ( 'NONE',  ( 0.000000000000000000, 0.000000000000000000, 1.000000000000000000 ) ) ;
#18423=AXIS2_PLACEMENT_3D ( 'NONE', #9991, #11366, #14598 ) ;
#18424=VERTEX_POINT ( 'NONE', #19100 ) ;
#18453=AXIS2_PLACEMENT_3D ( 'NONE', #8969, #16242, #1240 ) ;
#18489=DIRECTION ( 'NONE',  ( -1.000000000000000000, -0.000000000000000000, -0.000000000000000000 ) ) ;
#18491=AXIS2_PLACEMENT_3D ( 'NONE', #15114, #314, #6289 ) ;
#18503=ORIENTED_EDGE ( 'NONE', *, *, #18999, .F. ) ;
#18604=ORIENTED_EDGE ( 'NONE', *, *, #10749, .T. ) ;
#18618=DIRECTION ( 'NONE',  ( -1.000000000000000000, -0.000000000000000000, -0.000000000000000000 ) ) ;
#18627=EDGE_LOOP ( 'NONE', ( #16438, #4472, #12691, #15418, #16671 ) ) ;
#18629=CARTESIAN_POINT ( 'NONE',  ( 0.1999999999999987899, 0.000000000000000000, 0.000000000000000000 ) ) ;
#18684=ORIENTED_EDGE ( 'NONE', *, *, #17190, .F. ) ;
#18783=VERTEX_POINT ( 'NONE', #14140 ) ;
#18811=DIRECTION ( 'NONE',  ( 0.000000000000000000, 0.000000000000000000, 1.000000000000000000 ) ) ;
#18813=ORIENTED_EDGE ( 'NONE', *, *, #11351, .T. ) ;
#18821=CIRCLE ( 'NONE', #18491, 2.200000000000001066 ) ;
#18824=CARTESIAN_POINT ( 'NONE',  ( -31.74999999999995737, 0.000000000000000000, 3.500000000000000000 ) ) ;
#18892=DIRECTION ( 'NONE',  ( 0.000000000000000000, -1.000000000000000000, 9.783878858594328898E-16 ) ) ;
#18908=ORIENTED_EDGE ( 'NONE', *, *, #14784, .T. ) ;
#18916=VERTEX_POINT ( 'NONE', #920 ) ;
#18918=ORIENTED_EDGE ( 'NONE', *, *, #11192, .T. ) ;
#18942=VECTOR ( 'NONE', #12957, 1000.000000000000114 ) ;
#18979=DIRECTION ( 'NONE',  ( 0.000000000000000000, 0.000000000000000000, 1.000000000000000000 ) ) ;
#18999=EDGE_CURVE ( 'NONE', #4627, #3135, #14723, .T. ) ;
#19100=CARTESIAN_POINT ( 'NONE',  ( 13.99999999999999822, 2.210487472460973684E-16, -1.610000000000000098 ) ) ;
#19102=EDGE_CURVE ( 'NONE', #18783, #8359, #17785, .T. ) ;
#19158=AXIS2_PLACEMENT_3D ( 'NONE', #14927, #4157, #1503 ) ;
#19178=DIRECTION ( 'NONE',  ( 0.000000000000000000, 1.000000000000000000, -1.345283343056720273E-15 ) ) ;
#19207=VECTOR ( 'NONE', #4758, 1000.000000000000000 ) ;
#19246=DIRECTION ( 'NONE',  ( 0.000000000000000000, 0.000000000000000000, 1.000000000000000000 ) ) ;
#19273=CARTESIAN_POINT ( 'NONE',  ( 2.000000000000000000, -0.8865213383406694847, 1.535500000000001419 ) ) ;
#19336=ORIENTED_EDGE ( 'NONE', *, *, #10821, .T. ) ;
#19351=LINE ( 'NONE', #1479, #2742 ) ;
#19370=EDGE_CURVE ( 'NONE', #440, #6090, #12852, .T. ) ;
#19391=CARTESIAN_POINT ( 'NONE',  ( 2.000000000000000000, -0.8865213383406694847, 1.535500000000001419 ) ) ;
#19392=CIRCLE ( 'NONE', #14974, 0.2000000000000000944 ) ;
#19411=EDGE_LOOP ( 'NONE', ( #10537, #6416 ) ) ;
#19469=COLOUR_RGB('Black',0.12,0.14,0.17);
#19470=FILL_AREA_STYLE_COLOUR('',#19469);
#19471=FILL_AREA_STYLE('',(#19470));
#19472=SURFACE_STYLE_FILL_AREA(#19471);
#19473=SURFACE_SIDE_STYLE('',(#19472));
#19474=SURFACE_STYLE_USAGE(.BOTH.,#19473);
#19475=PRESENTATION_STYLE_ASSIGNMENT((#19474));
ENDSEC;
END-ISO-10303-21;
